ISO-10303-21;
HEADER;
FILE_DESCRIPTION (('STEP AP214'),
    '1' );
FILE_NAME ('socket head cap screw_iso_ISO 4762 M10 x 90 - 32N.step',
    '2026-10-08T07:58:12',
    ( '' ),
    ( '' ),
    'SwSTEP 2.0',
    'SolidWorks 2026',
    '' );
FILE_SCHEMA (( 'AUTOMOTIVE_DESIGN' ));
ENDSEC;

DATA;
#87=DIRECTION ( 'NONE',  ( 0.000000000000000000, -1.000000000000000000, 0.000000000000000000 ) ) ;
#175=LINE ( 'NONE', #28457, #23884 ) ;
#203=DIRECTION ( 'NONE',  ( 0.000000000000000000, 0.000000000000000000, 1.000000000000000000 ) ) ;
#328=ORIENTED_EDGE ( 'NONE', *, *, #21858, .T. ) ;
#408=DIRECTION ( 'NONE',  ( 0.000000000000000000, 0.000000000000000000, 1.000000000000000000 ) ) ;
#416=CIRCLE ( 'NONE', #9651, 5.000000000000000888 ) ;
#425=VECTOR ( 'NONE', #6795, 1000.000000000000227 ) ;
#481=VECTOR ( 'NONE', #17231, 1000.000000000000000 ) ;
#491=ORIENTED_EDGE ( 'NONE', *, *, #10155, .T. ) ;
#572=ORIENTED_EDGE ( 'NONE', *, *, #18867, .F. ) ;
#663=STYLED_ITEM ( 'NONE', ( #5034 ), #1878 ) ;
#683=LINE ( 'NONE', #11086, #20111 ) ;
#698=CIRCLE ( 'NONE', #9954, 4.057500000000000107 ) ;
#705=ORIENTED_EDGE ( 'NONE', *, *, #23746, .F. ) ;
#739=VERTEX_POINT ( 'NONE', #3543 ) ;
#831=DIRECTION ( 'NONE',  ( -1.000000000000000000, -0.000000000000000000, -0.000000000000000000 ) ) ;
#863=EDGE_CURVE ( 'NONE', #32863, #21974, #12924, .T. ) ;
#890=DIRECTION ( 'NONE',  ( -1.000000000000000000, -0.000000000000000000, -0.000000000000000000 ) ) ;
#908=FACE_OUTER_BOUND ( 'NONE', #23376, .T. ) ;
#991=CARTESIAN_POINT ( 'NONE',  ( 5.000000000000000000, -2.342598717236903383, 4.057500000000001883 ) ) ;
#1002=CARTESIAN_POINT ( 'NONE',  ( 99.17200000000002547, 0.000000000000000000, 5.000000000000000888 ) ) ;
#1014=CARTESIAN_POINT ( 'NONE',  ( 99.17200000000002547, 0.000000000000000000, 0.000000000000000000 ) ) ;
#1044=VERTEX_POINT ( 'NONE', #2517 ) ;
#1147=DIRECTION ( 'NONE',  ( 0.000000000000000000, -0.5000000000000014433, -0.8660254037844379305 ) ) ;
#1226=LINE ( 'NONE', #11624, #13011 ) ;
#1247=CARTESIAN_POINT ( 'NONE',  ( 99.99999999999998579, 0.000000000000000000, 0.000000000000000000 ) ) ;
#1250=DIRECTION ( 'NONE',  ( 1.000000000000000000, 0.000000000000000000, 0.000000000000000000 ) ) ;
#1264=LINE ( 'NONE', #22553, #33601 ) ;
#1289=SHAPE_REPRESENTATION ( 'socket head cap screw_iso_ISO 4762 M10 x 90 - 32N', ( #2404 ), #25772 ) ;
#1338=FACE_OUTER_BOUND ( 'NONE', #3579, .T. ) ;
#1350=CARTESIAN_POINT ( 'NONE',  ( 99.99999999999998579, 4.171999999999999709, 0.000000000000000000 ) ) ;
#1435=EDGE_CURVE ( 'NONE', #18587, #26841, #4226, .T. ) ;
#1438=CONICAL_SURFACE ( 'NONE', #19943, 4.057500000000000107, 1.047197551196593857 ) ;
#1439=ORIENTED_EDGE ( 'NONE', *, *, #8775, .F. ) ;
#1536=ORIENTED_EDGE ( 'NONE', *, *, #15348, .F. ) ;
#1542=ORIENTED_EDGE ( 'NONE', *, *, #8231, .F. ) ;
#1563=FACE_BOUND ( 'NONE', #24828, .T. ) ;
#1568=FACE_OUTER_BOUND ( 'NONE', #10760, .T. ) ;
#1650=EDGE_LOOP ( 'NONE', ( #21855, #8372 ) ) ;
#1661=EDGE_CURVE ( 'NONE', #21974, #31163, #33651, .T. ) ;
#1739=TOROIDAL_SURFACE ( 'NONE', #20227, 5.400000000000002132, 0.4000000000000000222 ) ;
#1781=DIRECTION ( 'NONE',  ( 0.000000000000000000, 0.8660254037844379305, -0.5000000000000014433 ) ) ;
#1839=AXIS2_PLACEMENT_3D ( 'NONE', #32751, #17255, #22197 ) ;
#1856=LINE ( 'NONE', #6799, #28999 ) ;
#1878=ADVANCED_BREP_SHAPE_REPRESENTATION ( '', ( #12506, #2404 ), #25772 ) ;
#1906=EDGE_LOOP ( 'NONE', ( #30932, #13807 ) ) ;
#1908=PRODUCT_DEFINITION ( 'UNKNOWN', '', #31143, #19299 ) ;
#1926=FACE_OUTER_BOUND ( 'NONE', #26468, .T. ) ;
#1970=( LENGTH_UNIT ( ) NAMED_UNIT ( * ) SI_UNIT ( .MILLI., .METRE. ) );
#1994=ORIENTED_EDGE ( 'NONE', *, *, #18228, .F. ) ;
#2007=DIRECTION ( 'NONE',  ( -1.000000000000000000, -0.000000000000000000, -0.000000000000000000 ) ) ;
#2117=EDGE_CURVE ( 'NONE', #11134, #6637, #15716, .T. ) ;
#2318=DIRECTION ( 'NONE',  ( 0.000000000000000000, 0.000000000000000000, 1.000000000000000000 ) ) ;
#2404=AXIS2_PLACEMENT_3D ( 'NONE', #8872, #11941, #4266 ) ;
#2408=PLANE ( 'NONE',  #12067 ) ;
#2418=ORIENTED_EDGE ( 'NONE', *, *, #32627, .T. ) ;
#2434=ORIENTED_EDGE ( 'NONE', *, *, #20489, .T. ) ;
#2462=DIRECTION ( 'NONE',  ( -0.000000000000000000, 0.000000000000000000, 1.000000000000000000 ) ) ;
#2478=EDGE_CURVE ( 'NONE', #28367, #26329, #175, .T. ) ;
#2517=CARTESIAN_POINT ( 'NONE',  ( 5.000000000000000000, -2.342598717236912265, -4.057499999999995666 ) ) ;
#2569=CARTESIAN_POINT ( 'NONE',  ( 0.000000000000000000, -4.685197434473814759, 3.903127820947815962E-15 ) ) ;
#2822=AXIS2_PLACEMENT_3D ( 'NONE', #32750, #4651, #32925 ) ;
#2842=ADVANCED_FACE ( 'NONE', ( #10900 ), #13624, .T. ) ;
#2881=VERTEX_POINT ( 'NONE', #19227 ) ;
#3051=DIRECTION ( 'NONE',  ( 0.000000000000000000, 1.000000000000000000, -1.295896757998781572E-15 ) ) ;
#3098=ADVANCED_FACE ( 'NONE', ( #30466 ), #7305, .T. ) ;
#3243=CARTESIAN_POINT ( 'NONE',  ( 0.000000000000000000, 4.685197434473814759, -5.637851296924623057E-15 ) ) ;
#3395=AXIS2_PLACEMENT_3D ( 'NONE', #27713, #7444, #17660 ) ;
#3413=VECTOR ( 'NONE', #32433, 1000.000000000000000 ) ;
#3463=STYLED_ITEM ( 'NONE', ( #15005 ), #12506 ) ;
#3531=ORIENTED_EDGE ( 'NONE', *, *, #28929, .T. ) ;
#3543=CARTESIAN_POINT ( 'NONE',  ( 5.000000000000000000, 2.342598717236900718, -4.057500000000001883 ) ) ;
#3568=DIRECTION ( 'NONE',  ( -1.000000000000000000, -0.000000000000000000, -0.000000000000000000 ) ) ;
#3576=DIRECTION ( 'NONE',  ( 0.000000000000000000, 0.4999999999999993339, -0.8660254037844389297 ) ) ;
#3579=EDGE_LOOP ( 'NONE', ( #32085, #32235, #28616 ) ) ;
#3622=UNCERTAINTY_MEASURE_WITH_UNIT (LENGTH_MEASURE( 1.000000000000000082E-05 ), #9632, 'distance_accuracy_value', 'NONE');
#3703=CIRCLE ( 'NONE', #5858, 6.500000000000000888 ) ;
#3765=ORIENTED_EDGE ( 'NONE', *, *, #2478, .F. ) ;
#3851=PLANE ( 'NONE',  #6445 ) ;
#3872=VERTEX_POINT ( 'NONE', #33108 ) ;
#3902=VECTOR ( 'NONE', #17593, 1000.000000000000114 ) ;
#3909=EDGE_LOOP ( 'NONE', ( #27508, #11386, #9455, #19595 ) ) ;
#3929=AXIS2_PLACEMENT_3D ( 'NONE', #14507, #29858, #32733 ) ;
#3933=ADVANCED_FACE ( 'NONE', ( #15045 ), #19988, .T. ) ;
#3961=ORIENTED_EDGE ( 'NONE', *, *, #7063, .T. ) ;
#4113=ORIENTED_EDGE ( 'NONE', *, *, #7462, .T. ) ;
#4116=CARTESIAN_POINT ( 'NONE',  ( 5.000000000000000000, -2.342598717236903383, 4.057500000000001883 ) ) ;
#4159=DIRECTION ( 'NONE',  ( -1.000000000000000000, -0.000000000000000000, -0.000000000000000000 ) ) ;
#4226=CIRCLE ( 'NONE', #29797, 5.000000000000001776 ) ;
#4266=DIRECTION ( 'NONE',  ( 1.000000000000000000, 0.000000000000000000, 0.000000000000000000 ) ) ;
#4322=CARTESIAN_POINT ( 'NONE',  ( 5.000000000000000000, 4.685197434473814759, -5.637851296924623057E-15 ) ) ;
#4345=CARTESIAN_POINT ( 'NONE',  ( 5.000000000000000000, 4.685197434473814759, -5.637851296924623057E-15 ) ) ;
#4380=ORIENTED_EDGE ( 'NONE', *, *, #23746, .T. ) ;
#4459=LINE ( 'NONE', #4116, #6344 ) ;
#4643=DIRECTION ( 'NONE',  ( 1.000000000000000000, 0.000000000000000000, 0.000000000000000000 ) ) ;
#4651=DIRECTION ( 'NONE',  ( 0.000000000000000000, 0.8660254037844381525, -0.5000000000000008882 ) ) ;
#4772=DIRECTION ( 'NONE',  ( 0.000000000000000000, -0.8660254037844390407, -0.4999999999999995004 ) ) ;
#4841=CARTESIAN_POINT ( 'NONE',  ( 0.000000000000000000, 0.000000000000000000, 0.000000000000000000 ) ) ;
#4847=ORIENTED_EDGE ( 'NONE', *, *, #25539, .F. ) ;
#4914=LINE ( 'NONE', #23313, #24730 ) ;
#4931=ADVANCED_FACE ( 'NONE', ( #7691 ), #2408, .F. ) ;
#5034=PRESENTATION_STYLE_ASSIGNMENT (( #17985 ) ) ;
#5147=VERTEX_POINT ( 'NONE', #7526 ) ;
#5175=DIRECTION ( 'NONE',  ( -1.000000000000000000, 0.000000000000000000, -0.000000000000000000 ) ) ;
#5190=FACE_OUTER_BOUND ( 'NONE', #27458, .T. ) ;
#5230=DIRECTION ( 'NONE',  ( 0.000000000000000000, -1.000000000000000000, 1.295896757998781966E-15 ) ) ;
#5259=CIRCLE ( 'NONE', #9047, 4.057500000000000107 ) ;
#5263=ORIENTED_EDGE ( 'NONE', *, *, #30605, .T. ) ;
#5330=TOROIDAL_SURFACE ( 'NONE', #23827, 5.400000000000002132, 0.4000000000000000222 ) ;
#5353=ORIENTED_EDGE ( 'NONE', *, *, #28885, .F. ) ;
#5363=EDGE_CURVE ( 'NONE', #20140, #14728, #29633, .T. ) ;
#5474=ORIENTED_EDGE ( 'NONE', *, *, #2117, .T. ) ;
#5698=ORIENTED_EDGE ( 'NONE', *, *, #6828, .F. ) ;
#5716=ORIENTED_EDGE ( 'NONE', *, *, #15535, .T. ) ;
#5756=ADVANCED_FACE ( 'NONE', ( #5190 ), #5330, .F. ) ;
#5757=CARTESIAN_POINT ( 'NONE',  ( 10.40000000000000036, 0.000000000000000000, 0.000000000000000000 ) ) ;
#5793=ORIENTED_EDGE ( 'NONE', *, *, #14291, .F. ) ;
#5814=EDGE_CURVE ( 'NONE', #25971, #22347, #33642, .T. ) ;
#5827=CARTESIAN_POINT ( 'NONE',  ( 1.500000000000001332, 0.000000000000000000, 0.000000000000000000 ) ) ;
#5858=AXIS2_PLACEMENT_3D ( 'NONE', #27282, #27120, #11616 ) ;
#6097=DIRECTION ( 'NONE',  ( -1.000000000000000000, -0.000000000000000000, -0.000000000000000000 ) ) ;
#6197=ADVANCED_FACE ( 'NONE', ( #21854 ), #19812, .F. ) ;
#6204=ADVANCED_FACE ( 'NONE', ( #11973 ), #9163, .F. ) ;
#6218=CARTESIAN_POINT ( 'NONE',  ( 5.000000000000000000, -4.685197434473814759, 3.903127820947815962E-15 ) ) ;
#6229=ADVANCED_FACE ( 'NONE', ( #908 ), #26572, .T. ) ;
#6263=DIRECTION ( 'NONE',  ( 0.000000000000000000, 0.000000000000000000, -1.000000000000000000 ) ) ;
#6280=DIRECTION ( 'NONE',  ( 0.000000000000000000, 1.000000000000000000, -1.295896757998781572E-15 ) ) ;
#6286=CARTESIAN_POINT ( 'NONE',  ( 10.40000000000000036, 6.613092715395709439E-16, 5.400000000000002132 ) ) ;
#6344=VECTOR ( 'NONE', #19458, 1000.000000000000000 ) ;
#6397=AXIS2_PLACEMENT_3D ( 'NONE', #14057, #19512, #24272 ) ;
#6445=AXIS2_PLACEMENT_3D ( 'NONE', #16296, #19027, #29752 ) ;
#6482=ADVANCED_FACE ( 'NONE', ( #8967 ), #3851, .F. ) ;
#6546=CARTESIAN_POINT ( 'NONE',  ( -31.74999999999995737, 0.000000000000000000, 8.000000000000000000 ) ) ;
#6611=CARTESIAN_POINT ( 'NONE',  ( 5.000000000000000000, 4.685197434473814759, -5.637851296924623057E-15 ) ) ;
#6628=EDGE_CURVE ( 'NONE', #16441, #26329, #18698, .T. ) ;
#6637=VERTEX_POINT ( 'NONE', #23970 ) ;
#6653=ORIENTED_EDGE ( 'NONE', *, *, #20985, .F. ) ;
#6698=CARTESIAN_POINT ( 'NONE',  ( 5.000000000000000000, 4.685197434473814759, -5.637851296924623057E-15 ) ) ;
#6744=DIRECTION ( 'NONE',  ( 1.000000000000000000, 0.000000000000000000, 0.000000000000000000 ) ) ;
#6768=ORIENTED_EDGE ( 'NONE', *, *, #8485, .T. ) ;
#6795=DIRECTION ( 'NONE',  ( 0.000000000000000000, -0.4999999999999994449, 0.8660254037844389297 ) ) ;
#6799=CARTESIAN_POINT ( 'NONE',  ( 0.000000000000000000, -2.342598717236903383, 4.057500000000001883 ) ) ;
#6828=EDGE_CURVE ( 'NONE', #25971, #15698, #21690, .T. ) ;
#6843=LINE ( 'NONE', #22341, #481 ) ;
#6855=DIRECTION ( 'NONE',  ( -0.000000000000000000, 1.000000000000000000, 1.224646799147353207E-16 ) ) ;
#6865=CARTESIAN_POINT ( 'NONE',  ( 10.40000000000000036, 0.000000000000000000, 0.000000000000000000 ) ) ;
#6899=PLANE ( 'NONE',  #21108 ) ;
#6946=DIRECTION ( 'NONE',  ( -1.000000000000000000, -0.000000000000000000, -0.000000000000000000 ) ) ;
#6954=CARTESIAN_POINT ( 'NONE',  ( 5.000000000000000000, 4.685197434473814759, -5.637851296924623057E-15 ) ) ;
#6988=VECTOR ( 'NONE', #18723, 1000.000000000000000 ) ;
#7047=CARTESIAN_POINT ( 'NONE',  ( 10.00000000000000178, 9.797174393178825657E-16, -8.000000000000000000 ) ) ;
#7063=EDGE_CURVE ( 'NONE', #6637, #11134, #10836, .T. ) ;
#7065=EDGE_LOOP ( 'NONE', ( #12126, #5698, #15288, #15233 ) ) ;
#7154=ORIENTED_EDGE ( 'NONE', *, *, #18474, .F. ) ;
#7211=DIRECTION ( 'NONE',  ( -1.000000000000000000, -0.000000000000000000, -0.000000000000000000 ) ) ;
#7235=LINE ( 'NONE', #32951, #31160 ) ;
#7305=PLANE ( 'NONE',  #32149 ) ;
#7307=CONICAL_SURFACE ( 'NONE', #9459, 4.171999999999999709, 0.7853981633974687071 ) ;
#7444=DIRECTION ( 'NONE',  ( 1.000000000000000000, 0.000000000000000000, 0.000000000000000000 ) ) ;
#7462=EDGE_CURVE ( 'NONE', #6637, #25971, #25279, .T. ) ;
#7464=EDGE_LOOP ( 'NONE', ( #24203, #18021, #17572, #27724 ) ) ;
#7485=CIRCLE ( 'NONE', #6397, 4.057500000000000107 ) ;
#7487=AXIS2_PLACEMENT_3D ( 'NONE', #32663, #2007, #29782 ) ;
#7507=AXIS2_PLACEMENT_3D ( 'NONE', #25724, #4772, #33565 ) ;
#7526=CARTESIAN_POINT ( 'NONE',  ( 10.00000000000000178, 0.000000000000000000, -5.400000000000002132 ) ) ;
#7544=CARTESIAN_POINT ( 'NONE',  ( 5.000000000000000000, 0.000000000000000000, 0.000000000000000000 ) ) ;
#7580=EDGE_LOOP ( 'NONE', ( #491, #16696, #2434, #19920 ) ) ;
#7624=EDGE_LOOP ( 'NONE', ( #7154, #11094, #19759, #328, #5716 ) ) ;
#7691=FACE_OUTER_BOUND ( 'NONE', #29821, .T. ) ;
#7742=CARTESIAN_POINT ( 'NONE',  ( 1.500000000000001332, 9.797174393178825657E-16, -8.000000000000000000 ) ) ;
#7780=VECTOR ( 'NONE', #3568, 1000.000000000000000 ) ;
#7808=ADVANCED_FACE ( 'NONE', ( #31566 ), #21180, .T. ) ;
#7871=AXIS2_PLACEMENT_3D ( 'NONE', #991, #21438, #21935 ) ;
#8045=ADVANCED_FACE ( 'NONE', ( #1563, #32393 ), #17230, .T. ) ;
#8089=CARTESIAN_POINT ( 'NONE',  ( 5.000000000000000000, 0.000000000000000000, 0.000000000000000000 ) ) ;
#8119=AXIS2_PLACEMENT_3D ( 'NONE', #14659, #17386, #25559 ) ;
#8136=AXIS2_PLACEMENT_3D ( 'NONE', #5827, #890, #11287 ) ;
#8231=EDGE_CURVE ( 'NONE', #32863, #13926, #19286, .T. ) ;
#8330=CARTESIAN_POINT ( 'NONE',  ( 5.000000000000000000, 2.342598717236900718, -4.057500000000001883 ) ) ;
#8372=ORIENTED_EDGE ( 'NONE', *, *, #2117, .F. ) ;
#8411=ORIENTED_EDGE ( 'NONE', *, *, #22871, .F. ) ;
#8434=DIRECTION ( 'NONE',  ( -1.000000000000000000, -0.000000000000000000, -0.000000000000000000 ) ) ;
#8479=DIRECTION ( 'NONE',  ( -1.000000000000000000, -0.000000000000000000, -0.000000000000000000 ) ) ;
#8485=EDGE_CURVE ( 'NONE', #28367, #29320, #683, .T. ) ;
#8515=DIRECTION ( 'NONE',  ( 0.000000000000000000, -0.5000000000000008882, -0.8660254037844381525 ) ) ;
#8567=CARTESIAN_POINT ( 'NONE',  ( 0.000000000000000000, 0.000000000000000000, 6.500000000000000888 ) ) ;
#8581=DIRECTION ( 'NONE',  ( 0.000000000000000000, 0.000000000000000000, -1.000000000000000000 ) ) ;
#8613=VERTEX_POINT ( 'NONE', #23851 ) ;
#8642=AXIS2_PLACEMENT_3D ( 'NONE', #13210, #8434, #11784 ) ;
#8775=EDGE_CURVE ( 'NONE', #18587, #25169, #24461, .T. ) ;
#8833=AXIS2_PLACEMENT_3D ( 'NONE', #4841, #5175, #2462 ) ;
#8838=DIRECTION ( 'NONE',  ( 0.000000000000000000, 0.000000000000000000, 1.000000000000000000 ) ) ;
#8872=CARTESIAN_POINT ( 'NONE',  ( 0.000000000000000000, 0.000000000000000000, 0.000000000000000000 ) ) ;
#8912=DIRECTION ( 'NONE',  ( 0.000000000000000000, 0.000000000000000000, 1.000000000000000000 ) ) ;
#8952=VERTEX_POINT ( 'NONE', #30655 ) ;
#8967=FACE_OUTER_BOUND ( 'NONE', #11646, .T. ) ;
#8984=CARTESIAN_POINT ( 'NONE',  ( 5.000000000000000000, 4.685197434473814759, -5.637851296924623057E-15 ) ) ;
#9047=AXIS2_PLACEMENT_3D ( 'NONE', #7544, #17576, #203 ) ;
#9057=CARTESIAN_POINT ( 'NONE',  ( 10.00000000000000178, 8.000000000000000000, 0.000000000000000000 ) ) ;
#9163=CONICAL_SURFACE ( 'NONE', #30409, 4.057500000000000107, 1.047197551196593857 ) ;
#9180=AXIS2_PLACEMENT_3D ( 'NONE', #15675, #12959, #30856 ) ;
#9233=CARTESIAN_POINT ( 'NONE',  ( 99.99999999999998579, 5.109226446042757607E-16, -4.171999999999999709 ) ) ;
#9253=CARTESIAN_POINT ( 'NONE',  ( 5.000000000000000000, -4.685197434473814759, 3.903127820947815962E-15 ) ) ;
#9281=DIRECTION ( 'NONE',  ( -0.5000000000000034417, 1.060575238724904696E-16, -0.8660254037844367092 ) ) ;
#9345=LINE ( 'NONE', #17183, #425 ) ;
#9425=FACE_OUTER_BOUND ( 'NONE', #22030, .T. ) ;
#9435=LINE ( 'NONE', #4322, #18895 ) ;
#9455=ORIENTED_EDGE ( 'NONE', *, *, #13283, .T. ) ;
#9459=AXIS2_PLACEMENT_3D ( 'NONE', #22485, #17542, #14474 ) ;
#9561=DIRECTION ( 'NONE',  ( 1.000000000000000000, 0.000000000000000000, 0.000000000000000000 ) ) ;
#9573=CARTESIAN_POINT ( 'NONE',  ( 1.500000000000001332, 7.960204194457796463E-16, -6.500000000000000888 ) ) ;
#9632=( LENGTH_UNIT ( ) NAMED_UNIT ( * ) SI_UNIT ( .MILLI., .METRE. ) );
#9637=CARTESIAN_POINT ( 'NONE',  ( 1.500000000000001332, 0.000000000000000000, 0.000000000000000000 ) ) ;
#9651=AXIS2_PLACEMENT_3D ( 'NONE', #16661, #831, #11221 ) ;
#9674=DIRECTION ( 'NONE',  ( 0.000000000000000000, -0.4999999999999993339, 0.8660254037844389297 ) ) ;
#9717=ORIENTED_EDGE ( 'NONE', *, *, #1435, .F. ) ;
#9842=ORIENTED_EDGE ( 'NONE', *, *, #18474, .T. ) ;
#9902=AXIS2_PLACEMENT_3D ( 'NONE', #9992, #14924, #30944 ) ;
#9954=AXIS2_PLACEMENT_3D ( 'NONE', #14550, #11996, #20002 ) ;
#9992=CARTESIAN_POINT ( 'NONE',  ( 0.000000000000000000, 0.000000000000000000, 0.000000000000000000 ) ) ;
#9998=ADVANCED_FACE ( 'NONE', ( #12952 ), #26222, .T. ) ;
#10066=ORIENTED_EDGE ( 'NONE', *, *, #16616, .F. ) ;
#10154=CARTESIAN_POINT ( 'NONE',  ( 5.000000000000000000, 3.513898075855361292, 2.028749999999997833 ) ) ;
#10155=EDGE_CURVE ( 'NONE', #31163, #13926, #416, .T. ) ;
#10159=FACE_OUTER_BOUND ( 'NONE', #3909, .T. ) ;
#10243=ORIENTED_EDGE ( 'NONE', *, *, #17718, .T. ) ;
#10390=ADVANCED_FACE ( 'NONE', ( #1338 ), #22283, .F. ) ;
#10548=AXIS2_PLACEMENT_3D ( 'NONE', #9573, #6855, #20139 ) ;
#10606=ORIENTED_EDGE ( 'NONE', *, *, #7462, .F. ) ;
#10646=EDGE_LOOP ( 'NONE', ( #3531, #16769, #2418, #28542, #6653, #5793 ) ) ;
#10650=CARTESIAN_POINT ( 'NONE',  ( 1.500000000000001332, 0.000000000000000000, 6.500000000000000888 ) ) ;
#10760=EDGE_LOOP ( 'NONE', ( #10928, #5474, #4113, #30189 ) ) ;
#10774=CIRCLE ( 'NONE', #31982, 5.000000000000000888 ) ;
#10817=ORIENTED_EDGE ( 'NONE', *, *, #19154, .T. ) ;
#10836=CIRCLE ( 'NONE', #17913, 8.000000000000000000 ) ;
#10887=ORIENTED_EDGE ( 'NONE', *, *, #22513, .F. ) ;
#10900=FACE_OUTER_BOUND ( 'NONE', #7065, .T. ) ;
#10928=ORIENTED_EDGE ( 'NONE', *, *, #30829, .F. ) ;
#11058=PLANE ( 'NONE',  #7871 ) ;
#11068=AXIS2_PLACEMENT_3D ( 'NONE', #30028, #4643, #28151 ) ;
#11086=CARTESIAN_POINT ( 'NONE',  ( 5.000000000000000000, -2.342598717236903383, 4.057500000000001883 ) ) ;
#11094=ORIENTED_EDGE ( 'NONE', *, *, #6628, .T. ) ;
#11118=( GEOMETRIC_REPRESENTATION_CONTEXT ( 3 ) GLOBAL_UNCERTAINTY_ASSIGNED_CONTEXT ( ( #26349 ) ) GLOBAL_UNIT_ASSIGNED_CONTEXT ( ( #32551, #24893, #19946 ) ) REPRESENTATION_CONTEXT ( 'NONE', 'WORKASPACE' ) );
#11134=VERTEX_POINT ( 'NONE', #7047 ) ;
#11216=FACE_OUTER_BOUND ( 'NONE', #32702, .T. ) ;
#11221=DIRECTION ( 'NONE',  ( 0.000000000000000000, 0.000000000000000000, 1.000000000000000000 ) ) ;
#11287=DIRECTION ( 'NONE',  ( 0.000000000000000000, 0.000000000000000000, 1.000000000000000000 ) ) ;
#11297=CARTESIAN_POINT ( 'NONE',  ( 10.40000000000000036, 0.000000000000000000, -5.400000000000002132 ) ) ;
#11308=VERTEX_POINT ( 'NONE', #25778 ) ;
#11379=EDGE_LOOP ( 'NONE', ( #32707, #14174, #31266, #32947, #33520 ) ) ;
#11386=ORIENTED_EDGE ( 'NONE', *, *, #28885, .T. ) ;
#11512=EDGE_LOOP ( 'NONE', ( #19876, #24314, #705, #29570, #15605 ) ) ;
#11548=LINE ( 'NONE', #22276, #16219 ) ;
#11616=DIRECTION ( 'NONE',  ( 0.000000000000000000, 0.000000000000000000, 1.000000000000000000 ) ) ;
#11624=CARTESIAN_POINT ( 'NONE',  ( 5.000000000000000000, -2.342598717236903383, 4.057500000000001883 ) ) ;
#11629=CYLINDRICAL_SURFACE ( 'NONE', #3929, 8.000000000000000000 ) ;
#11646=EDGE_LOOP ( 'NONE', ( #4380, #10243, #22646 ) ) ;
#11784=DIRECTION ( 'NONE',  ( 0.000000000000000000, 0.000000000000000000, 1.000000000000000000 ) ) ;
#11795=VECTOR ( 'NONE', #30104, 999.9999999999998863 ) ;
#11858=AXIS2_PLACEMENT_3D ( 'NONE', #1350, #32514, #20081 ) ;
#11941=DIRECTION ( 'NONE',  ( 0.000000000000000000, 0.000000000000000000, 1.000000000000000000 ) ) ;
#11973=FACE_OUTER_BOUND ( 'NONE', #12216, .T. ) ;
#11974=VERTEX_POINT ( 'NONE', #2569 ) ;
#11976=PLANE ( 'NONE',  #2822 ) ;
#11996=DIRECTION ( 'NONE',  ( -1.000000000000000000, -0.000000000000000000, -0.000000000000000000 ) ) ;
#12067=AXIS2_PLACEMENT_3D ( 'NONE', #25905, #18410, #28802 ) ;
#12076=DIRECTION ( 'NONE',  ( 0.000000000000000000, -0.4999999999999994449, 0.8660254037844389297 ) ) ;
#12092=ADVANCED_FACE ( 'NONE', ( #27478 ), #22362, .T. ) ;
#12126=ORIENTED_EDGE ( 'NONE', *, *, #19348, .F. ) ;
#12149=CARTESIAN_POINT ( 'NONE',  ( -31.74999999999995737, 9.797174393178825657E-16, -8.000000000000000000 ) ) ;
#12151=PRODUCT_DEFINITION_SHAPE ( 'NONE', 'NONE',  #1908 ) ;
#12216=EDGE_LOOP ( 'NONE', ( #20726, #9842, #24662, #19932, #26745 ) ) ;
#12384=ORIENTED_EDGE ( 'NONE', *, *, #17718, .F. ) ;
#12413=FACE_OUTER_BOUND ( 'NONE', #1906, .T. ) ;
#12506=MANIFOLD_SOLID_BREP ( 'Hex', #15589 ) ;
#12510=FACE_BOUND ( 'NONE', #10646, .T. ) ;
#12536=DIRECTION ( 'NONE',  ( -1.000000000000000000, -0.000000000000000000, -0.000000000000000000 ) ) ;
#12616=VECTOR ( 'NONE', #12648, 999.9999999999998863 ) ;
#12648=DIRECTION ( 'NONE',  ( 0.000000000000000000, -0.5000000000000014433, -0.8660254037844379305 ) ) ;
#12835=DIRECTION ( 'NONE',  ( 0.000000000000000000, 0.000000000000000000, 1.000000000000000000 ) ) ;
#12924=CIRCLE ( 'NONE', #7487, 4.171999999999999709 ) ;
#12952=FACE_OUTER_BOUND ( 'NONE', #11379, .T. ) ;
#12959=DIRECTION ( 'NONE',  ( -1.000000000000000000, -0.000000000000000000, -0.000000000000000000 ) ) ;
#13011=VECTOR ( 'NONE', #30015, 1000.000000000000000 ) ;
#13042=VECTOR ( 'NONE', #19623, 1000.000000000000000 ) ;
#13067=ORIENTED_EDGE ( 'NONE', *, *, #18228, .T. ) ;
#13103=AXIS2_PLACEMENT_3D ( 'NONE', #21448, #6097, #19391 ) ;
#13210=CARTESIAN_POINT ( 'NONE',  ( 5.000000000000000000, 0.000000000000000000, 0.000000000000000000 ) ) ;
#13228=ORIENTED_EDGE ( 'NONE', *, *, #19348, .T. ) ;
#13283=EDGE_CURVE ( 'NONE', #31163, #18587, #4914, .T. ) ;
#13519=AXIS2_PLACEMENT_3D ( 'NONE', #6698, #32245, #29529 ) ;
#13624=TOROIDAL_SURFACE ( 'NONE', #13103, 6.500000000000000888, 1.500000000000000000 ) ;
#13762=ADVANCED_FACE ( 'NONE', ( #10159 ), #17814, .T. ) ;
#13807=ORIENTED_EDGE ( 'NONE', *, *, #863, .F. ) ;
#13835=EDGE_CURVE ( 'NONE', #2881, #22347, #24582, .T. ) ;
#13886=ORIENTED_EDGE ( 'NONE', *, *, #24164, .F. ) ;
#13926=VERTEX_POINT ( 'NONE', #14369 ) ;
#13969=AXIS2_PLACEMENT_3D ( 'NONE', #6954, #33005, #19727 ) ;
#13973=EDGE_CURVE ( 'NONE', #20097, #1044, #14696, .T. ) ;
#13976=ORIENTED_EDGE ( 'NONE', *, *, #18516, .F. ) ;
#14057=CARTESIAN_POINT ( 'NONE',  ( 5.000000000000000000, 0.000000000000000000, 0.000000000000000000 ) ) ;
#14084=CIRCLE ( 'NONE', #9180, 5.400000000000002132 ) ;
#14099=ADVANCED_FACE ( 'NONE', ( #1926 ), #11976, .T. ) ;
#14109=ADVANCED_FACE ( 'NONE', ( #22361 ), #1739, .F. ) ;
#14140=ORIENTED_EDGE ( 'NONE', *, *, #8775, .T. ) ;
#14174=ORIENTED_EDGE ( 'NONE', *, *, #21659, .F. ) ;
#14193=CARTESIAN_POINT ( 'NONE',  ( 5.000000000000000000, 0.000000000000000000, 0.000000000000000000 ) ) ;
#14291=EDGE_CURVE ( 'NONE', #22951, #22562, #31386, .T. ) ;
#14311=VERTEX_POINT ( 'NONE', #28159 ) ;
#14369=CARTESIAN_POINT ( 'NONE',  ( 99.17200000000002547, 6.123233995736768255E-16, -5.000000000000000888 ) ) ;
#14464=ORIENTED_EDGE ( 'NONE', *, *, #30138, .F. ) ;
#14474=DIRECTION ( 'NONE',  ( 0.000000000000000000, 0.000000000000000000, 1.000000000000000000 ) ) ;
#14507=CARTESIAN_POINT ( 'NONE',  ( -31.74999999999995737, 0.000000000000000000, 0.000000000000000000 ) ) ;
#14550=CARTESIAN_POINT ( 'NONE',  ( 5.000000000000000000, 0.000000000000000000, 0.000000000000000000 ) ) ;
#14635=DIRECTION ( 'NONE',  ( 0.000000000000000000, 1.000000000000000000, -1.224646799147353207E-16 ) ) ;
#14659=CARTESIAN_POINT ( 'NONE',  ( 10.00000000000000178, 0.000000000000000000, 0.000000000000000000 ) ) ;
#14671=CARTESIAN_POINT ( 'NONE',  ( 5.000000000000000000, -2.342598717236903383, 4.057500000000001883 ) ) ;
#14696=LINE ( 'NONE', #9253, #3902 ) ;
#14717=ORIENTED_EDGE ( 'NONE', *, *, #19154, .F. ) ;
#14728=VERTEX_POINT ( 'NONE', #21907 ) ;
#14906=DIRECTION ( 'NONE',  ( 0.000000000000000000, 0.000000000000000000, -1.000000000000000000 ) ) ;
#14924=DIRECTION ( 'NONE',  ( -1.000000000000000000, -0.000000000000000000, -0.000000000000000000 ) ) ;
#14946=ORIENTED_EDGE ( 'NONE', *, *, #13835, .T. ) ;
#15005=PRESENTATION_STYLE_ASSIGNMENT (( #33238 ) ) ;
#15045=FACE_OUTER_BOUND ( 'NONE', #7580, .T. ) ;
#15087=CARTESIAN_POINT ( 'NONE',  ( -31.74999999999995737, 0.000000000000000000, 0.000000000000000000 ) ) ;
#15110=ORIENTED_EDGE ( 'NONE', *, *, #17467, .F. ) ;
#15114=CARTESIAN_POINT ( 'NONE',  ( 0.000000000000000000, 2.342598717236900718, -4.057500000000001883 ) ) ;
#15190=ORIENTED_EDGE ( 'NONE', *, *, #32404, .F. ) ;
#15194=DIRECTION ( 'NONE',  ( 0.000000000000000000, 0.000000000000000000, 1.000000000000000000 ) ) ;
#15227=ORIENTED_EDGE ( 'NONE', *, *, #22513, .T. ) ;
#15233=ORIENTED_EDGE ( 'NONE', *, *, #13835, .F. ) ;
#15288=ORIENTED_EDGE ( 'NONE', *, *, #5814, .T. ) ;
#15348=EDGE_CURVE ( 'NONE', #28367, #20140, #17113, .T. ) ;
#15362=COLOUR_RGB ( '', 0.31764706, 0.68627451, 0.89019608) ;
#15404=CARTESIAN_POINT ( 'NONE',  ( 5.000000000000000000, 2.342598717236900718, -4.057500000000001883 ) ) ;
#15424=SHAPE_REPRESENTATION_RELATIONSHIP ( 'NONE' , 'NONE' ,  #1289, #1878 ) ;
#15460=LINE ( 'NONE', #15114, #19207 ) ;
#15495=VERTEX_POINT ( 'NONE', #17445 ) ;
#15496=CARTESIAN_POINT ( 'NONE',  ( 10.00000000000000178, 6.613092715395708453E-16, 5.400000000000002132 ) ) ;
#15535=EDGE_CURVE ( 'NONE', #8952, #8613, #698, .T. ) ;
#15589=CLOSED_SHELL ( 'NONE', ( #6204, #7808, #14109, #19890, #3933, #12092, #15815, #16207, #8045, #13762, #6229, #28944, #5756, #2842, #9998, #20566, #14099, #3098, #4931, #24596, #16976, #31395, #30929, #6197, #10390, #6482, #22700 ) ) ;
#15605=ORIENTED_EDGE ( 'NONE', *, *, #21659, .T. ) ;
#15675=CARTESIAN_POINT ( 'NONE',  ( 10.00000000000000178, 0.000000000000000000, 0.000000000000000000 ) ) ;
#15698=VERTEX_POINT ( 'NONE', #7742 ) ;
#15716=CIRCLE ( 'NONE', #8119, 8.000000000000000000 ) ;
#15733=EDGE_LOOP ( 'NONE', ( #15227, #22706, #572 ) ) ;
#15815=ADVANCED_FACE ( 'NONE', ( #12510, #20344 ), #30743, .T. ) ;
#15995=AXIS2_PLACEMENT_3D ( 'NONE', #5757, #26882, #6263 ) ;
#16011=CARTESIAN_POINT ( 'NONE',  ( 0.000000000000000000, -2.342598717236903383, 4.057500000000001883 ) ) ;
#16109=CARTESIAN_POINT ( 'NONE',  ( 5.000000000000000000, 5.258101095580055525E-15, 4.057499999999999218 ) ) ;
#16164=VECTOR ( 'NONE', #1147, 999.9999999999998863 ) ;
#16207=ADVANCED_FACE ( 'NONE', ( #1568 ), #11629, .T. ) ;
#16219=VECTOR ( 'NONE', #6946, 1000.000000000000000 ) ;
#16253=CIRCLE ( 'NONE', #8642, 4.057500000000000107 ) ;
#16296=CARTESIAN_POINT ( 'NONE',  ( 5.000000000000000000, 4.685197434473814759, -5.637851296924623057E-15 ) ) ;
#16311=DIRECTION ( 'NONE',  ( 0.000000000000000000, 0.000000000000000000, 1.000000000000000000 ) ) ;
#16419=AXIS2_PLACEMENT_3D ( 'NONE', #15087, #23102, #33490 ) ;
#16441=VERTEX_POINT ( 'NONE', #30875 ) ;
#16528=ORIENTED_EDGE ( 'NONE', *, *, #28137, .T. ) ;
#16545=MECHANICAL_DESIGN_GEOMETRIC_PRESENTATION_REPRESENTATION('',(#3463),#11118);
#16555=ORIENTED_EDGE ( 'NONE', *, *, #32627, .F. ) ;
#16606=DIRECTION ( 'NONE',  ( -1.000000000000000000, -0.000000000000000000, -0.000000000000000000 ) ) ;
#16616=EDGE_CURVE ( 'NONE', #15495, #20097, #24194, .T. ) ;
#16661=CARTESIAN_POINT ( 'NONE',  ( 99.17200000000002547, 0.000000000000000000, 0.000000000000000000 ) ) ;
#16691=ORIENTED_EDGE ( 'NONE', *, *, #5363, .T. ) ;
#16696=ORIENTED_EDGE ( 'NONE', *, *, #25629, .T. ) ;
#16769=ORIENTED_EDGE ( 'NONE', *, *, #5363, .F. ) ;
#16814=CARTESIAN_POINT ( 'NONE',  ( 5.000000000000000000, 4.685197434473814759, -5.637851296924623057E-15 ) ) ;
#16817=ORIENTED_EDGE ( 'NONE', *, *, #30138, .T. ) ;
#16913=DIRECTION ( 'NONE',  ( 0.000000000000000000, 0.000000000000000000, -1.000000000000000000 ) ) ;
#16976=ADVANCED_FACE ( 'NONE', ( #30613 ), #17323, .F. ) ;
#16984=VECTOR ( 'NONE', #20689, 1000.000000000000000 ) ;
#17017=DIRECTION ( 'NONE',  ( 0.000000000000000000, -0.5000000000000008882, -0.8660254037844381525 ) ) ;
#17055=SURFACE_SIDE_STYLE ('',( #32720 ) ) ;
#17113=LINE ( 'NONE', #27497, #3413 ) ;
#17183=CARTESIAN_POINT ( 'NONE',  ( 0.000000000000000000, 4.685197434473814759, -5.637851296924623057E-15 ) ) ;
#17203=ORIENTED_EDGE ( 'NONE', *, *, #28137, .F. ) ;
#17230=PLANE ( 'NONE',  #28804 ) ;
#17231=DIRECTION ( 'NONE',  ( -1.000000000000000000, -0.000000000000000000, -0.000000000000000000 ) ) ;
#17255=DIRECTION ( 'NONE',  ( -1.000000000000000000, -0.000000000000000000, -0.000000000000000000 ) ) ;
#17323=PLANE ( 'NONE',  #3395 ) ;
#17337=AXIS2_PLACEMENT_3D ( 'NONE', #9637, #20032, #30432 ) ;
#17345=PLANE ( 'NONE',  #13969 ) ;
#17358=PLANE ( 'NONE',  #11858 ) ;
#17386=DIRECTION ( 'NONE',  ( -1.000000000000000000, -0.000000000000000000, -0.000000000000000000 ) ) ;
#17444=EDGE_CURVE ( 'NONE', #14311, #14728, #7235, .T. ) ;
#17445=CARTESIAN_POINT ( 'NONE',  ( 5.000000000000000000, -4.685197434473814759, 3.903127820947815962E-15 ) ) ;
#17467=EDGE_CURVE ( 'NONE', #11974, #3872, #27334, .T. ) ;
#17468=DIRECTION ( 'NONE',  ( 0.000000000000000000, 0.000000000000000000, -1.000000000000000000 ) ) ;
#17537=ORIENTED_EDGE ( 'NONE', *, *, #29987, .F. ) ;
#17542=DIRECTION ( 'NONE',  ( -1.000000000000000000, -0.000000000000000000, -0.000000000000000000 ) ) ;
#17572=ORIENTED_EDGE ( 'NONE', *, *, #10155, .F. ) ;
#17576=DIRECTION ( 'NONE',  ( -1.000000000000000000, -0.000000000000000000, -0.000000000000000000 ) ) ;
#17593=DIRECTION ( 'NONE',  ( 0.000000000000000000, 0.4999999999999993339, -0.8660254037844389297 ) ) ;
#17642=FILL_AREA_STYLE ('',( #20028 ) ) ;
#17660=DIRECTION ( 'NONE',  ( 0.000000000000000000, 0.000000000000000000, -1.000000000000000000 ) ) ;
#17683=CARTESIAN_POINT ( 'NONE',  ( 5.000000000000000000, -4.685197434473814759, 3.903127820947815962E-15 ) ) ;
#17718=EDGE_CURVE ( 'NONE', #739, #8613, #28360, .T. ) ;
#17784=CIRCLE ( 'NONE', #31921, 4.171999999999999709 ) ;
#17794=CARTESIAN_POINT ( 'NONE',  ( 10.40000000000000036, 0.000000000000000000, 5.000000000000001776 ) ) ;
#17814=CYLINDRICAL_SURFACE ( 'NONE', #16419, 5.000000000000001776 ) ;
#17865=CARTESIAN_POINT ( 'NONE',  ( 5.000000000000000000, -3.513898075855358183, 2.028750000000003606 ) ) ;
#17913=AXIS2_PLACEMENT_3D ( 'NONE', #28557, #12536, #2318 ) ;
#17928=VECTOR ( 'NONE', #27312, 1000.000000000000000 ) ;
#17937=ORIENTED_EDGE ( 'NONE', *, *, #20489, .F. ) ;
#17985=SURFACE_STYLE_USAGE ( .BOTH. , #28207 ) ;
#18021=ORIENTED_EDGE ( 'NONE', *, *, #8231, .T. ) ;
#18228=EDGE_CURVE ( 'NONE', #26841, #5147, #26810, .T. ) ;
#18368=DIRECTION ( 'NONE',  ( -1.000000000000000000, -0.000000000000000000, -0.000000000000000000 ) ) ;
#18410=DIRECTION ( 'NONE',  ( 0.000000000000000000, -1.295896757998781966E-15, -1.000000000000000000 ) ) ;
#18474=EDGE_CURVE ( 'NONE', #16441, #8613, #29906, .T. ) ;
#18516=EDGE_CURVE ( 'NONE', #15495, #11974, #21723, .T. ) ;
#18587=VERTEX_POINT ( 'NONE', #17794 ) ;
#18593=ORIENTED_EDGE ( 'NONE', *, *, #30216, .T. ) ;
#18698=LINE ( 'NONE', #32304, #18970 ) ;
#18719=ORIENTED_EDGE ( 'NONE', *, *, #863, .T. ) ;
#18723=DIRECTION ( 'NONE',  ( 0.000000000000000000, -1.000000000000000000, 1.295896757998781966E-15 ) ) ;
#18770=ORIENTED_EDGE ( 'NONE', *, *, #30829, .T. ) ;
#18799=DIRECTION ( 'NONE',  ( -1.000000000000000000, -0.000000000000000000, -0.000000000000000000 ) ) ;
#18867=EDGE_CURVE ( 'NONE', #26329, #26980, #32288, .T. ) ;
#18895=VECTOR ( 'NONE', #19992, 1000.000000000000227 ) ;
#18970=VECTOR ( 'NONE', #29087, 999.9999999999998863 ) ;
#19027=DIRECTION ( 'NONE',  ( 1.000000000000000000, 0.000000000000000000, 0.000000000000000000 ) ) ;
#19135=DIRECTION ( 'NONE',  ( -1.000000000000000000, -0.000000000000000000, -0.000000000000000000 ) ) ;
#19154=EDGE_CURVE ( 'NONE', #15698, #25971, #31731, .T. ) ;
#19207=VECTOR ( 'NONE', #5230, 1000.000000000000000 ) ;
#19227=CARTESIAN_POINT ( 'NONE',  ( 0.000000000000000000, 8.878689293818310074E-16, -6.500000000000000888 ) ) ;
#19286=LINE ( 'NONE', #9233, #13042 ) ;
#19294=DIRECTION ( 'NONE',  ( 0.000000000000000000, -1.000000000000000000, 0.000000000000000000 ) ) ;
#19299=PRODUCT_DEFINITION_CONTEXT ( 'detailed design', #22914, 'design' ) ;
#19348=EDGE_CURVE ( 'NONE', #15698, #2881, #21949, .T. ) ;
#19391=DIRECTION ( 'NONE',  ( 0.000000000000000000, 0.000000000000000000, 1.000000000000000000 ) ) ;
#19422=EDGE_LOOP ( 'NONE', ( #30397, #19599, #13886 ) ) ;
#19458=DIRECTION ( 'NONE',  ( 0.000000000000000000, 1.000000000000000000, -1.295896757998781572E-15 ) ) ;
#19479=DIRECTION ( 'NONE',  ( 0.000000000000000000, 0.000000000000000000, -1.000000000000000000 ) ) ;
#19512=DIRECTION ( 'NONE',  ( -1.000000000000000000, -0.000000000000000000, -0.000000000000000000 ) ) ;
#19595=ORIENTED_EDGE ( 'NONE', *, *, #1435, .T. ) ;
#19599=ORIENTED_EDGE ( 'NONE', *, *, #13973, .F. ) ;
#19623=DIRECTION ( 'NONE',  ( -0.7071067811865331398, 8.659560562355110352E-17, -0.7071067811865620056 ) ) ;
#19654=CARTESIAN_POINT ( 'NONE',  ( -31.74999999999995737, 0.000000000000000000, 0.000000000000000000 ) ) ;
#19723=DIRECTION ( 'NONE',  ( 1.000000000000000000, 0.000000000000000000, 0.000000000000000000 ) ) ;
#19727=DIRECTION ( 'NONE',  ( 0.000000000000000000, 0.000000000000000000, -1.000000000000000000 ) ) ;
#19759=ORIENTED_EDGE ( 'NONE', *, *, #18867, .T. ) ;
#19783=FILL_AREA_STYLE ('',( #22333 ) ) ;
#19812=PLANE ( 'NONE',  #13519 ) ;
#19819=PLANE ( 'NONE',  #25523 ) ;
#19831=DIRECTION ( 'NONE',  ( -1.000000000000000000, -0.000000000000000000, -0.000000000000000000 ) ) ;
#19876=ORIENTED_EDGE ( 'NONE', *, *, #14291, .T. ) ;
#19890=ADVANCED_FACE ( 'NONE', ( #25046 ), #7307, .T. ) ;
#19920=ORIENTED_EDGE ( 'NONE', *, *, #13283, .F. ) ;
#19932=ORIENTED_EDGE ( 'NONE', *, *, #29987, .T. ) ;
#19943=AXIS2_PLACEMENT_3D ( 'NONE', #28485, #23535, #15194 ) ;
#19946=( NAMED_UNIT ( * ) SI_UNIT ( $, .STERADIAN. ) SOLID_ANGLE_UNIT ( ) );
#19988=CYLINDRICAL_SURFACE ( 'NONE', #27825, 5.000000000000001776 ) ;
#19992=DIRECTION ( 'NONE',  ( 0.000000000000000000, -0.4999999999999994449, 0.8660254037844389297 ) ) ;
#20002=DIRECTION ( 'NONE',  ( 0.000000000000000000, 0.000000000000000000, 1.000000000000000000 ) ) ;
#20028=FILL_AREA_STYLE_COLOUR ( '', #15362 ) ;
#20032=DIRECTION ( 'NONE',  ( 1.000000000000000000, 0.000000000000000000, 0.000000000000000000 ) ) ;
#20038=AXIS2_PLACEMENT_3D ( 'NONE', #1247, #19135, #8912 ) ;
#20081=DIRECTION ( 'NONE',  ( 0.000000000000000000, 0.000000000000000000, -1.000000000000000000 ) ) ;
#20097=VERTEX_POINT ( 'NONE', #28103 ) ;
#20111=VECTOR ( 'NONE', #8515, 1000.000000000000000 ) ;
#20139=DIRECTION ( 'NONE',  ( 0.000000000000000000, -1.224646799147353454E-16, 1.000000000000000000 ) ) ;
#20140=VERTEX_POINT ( 'NONE', #22994 ) ;
#20227=AXIS2_PLACEMENT_3D ( 'NONE', #6865, #1250, #16913 ) ;
#20337=VECTOR ( 'NONE', #3576, 1000.000000000000114 ) ;
#20344=FACE_OUTER_BOUND ( 'NONE', #27376, .T. ) ;
#20361=CIRCLE ( 'NONE', #15995, 5.000000000000001776 ) ;
#20489=EDGE_CURVE ( 'NONE', #26841, #18587, #20361, .T. ) ;
#20504=CARTESIAN_POINT ( 'NONE',  ( 5.000000000000000000, 0.000000000000000000, 0.000000000000000000 ) ) ;
#20566=ADVANCED_FACE ( 'NONE', ( #11216 ), #11058, .F. ) ;
#20689=DIRECTION ( 'NONE',  ( 0.000000000000000000, -1.000000000000000000, 1.295896757998781966E-15 ) ) ;
#20726=ORIENTED_EDGE ( 'NONE', *, *, #6628, .F. ) ;
#20985=EDGE_CURVE ( 'NONE', #22562, #3872, #15460, .T. ) ;
#21108=AXIS2_PLACEMENT_3D ( 'NONE', #4345, #1781, #32957 ) ;
#21180=TOROIDAL_SURFACE ( 'NONE', #8136, 6.500000000000000888, 1.500000000000000000 ) ;
#21363=VECTOR ( 'NONE', #16606, 1000.000000000000000 ) ;
#21428=CARTESIAN_POINT ( 'NONE',  ( 99.99999999999998579, 0.000000000000000000, 0.000000000000000000 ) ) ;
#21438=DIRECTION ( 'NONE',  ( -0.000000000000000000, 1.295896757998781572E-15, 1.000000000000000000 ) ) ;
#21448=CARTESIAN_POINT ( 'NONE',  ( 1.500000000000001332, 0.000000000000000000, 0.000000000000000000 ) ) ;
#21477=ORIENTED_EDGE ( 'NONE', *, *, #5814, .F. ) ;
#21622=EDGE_CURVE ( 'NONE', #26980, #14311, #9435, .T. ) ;
#21659=EDGE_CURVE ( 'NONE', #11308, #22951, #1264, .T. ) ;
#21690=CIRCLE ( 'NONE', #17337, 8.000000000000000000 ) ;
#21692=DIRECTION ( 'NONE',  ( 0.000000000000000000, 0.000000000000000000, 1.000000000000000000 ) ) ;
#21723=LINE ( 'NONE', #6218, #21363 ) ;
#21760=ORIENTED_EDGE ( 'NONE', *, *, #18516, .T. ) ;
#21854=FACE_OUTER_BOUND ( 'NONE', #15733, .T. ) ;
#21855=ORIENTED_EDGE ( 'NONE', *, *, #7063, .F. ) ;
#21858=EDGE_CURVE ( 'NONE', #26980, #8952, #25910, .T. ) ;
#21907=CARTESIAN_POINT ( 'NONE',  ( 0.000000000000000000, 2.342598717236910488, 4.057499999999995666 ) ) ;
#21935=DIRECTION ( 'NONE',  ( 0.000000000000000000, -1.000000000000000000, 1.295896757998781572E-15 ) ) ;
#21949=CIRCLE ( 'NONE', #10548, 1.499999999999999556 ) ;
#21974=VERTEX_POINT ( 'NONE', #23226 ) ;
#22030=EDGE_LOOP ( 'NONE', ( #28055, #27307, #8411 ) ) ;
#22197=DIRECTION ( 'NONE',  ( 0.000000000000000000, 0.000000000000000000, 1.000000000000000000 ) ) ;
#22198=AXIS2_PLACEMENT_3D ( 'NONE', #10650, #87, #8581 ) ;
#22276=CARTESIAN_POINT ( 'NONE',  ( -31.74999999999995737, 6.123233995736768255E-16, -5.000000000000001776 ) ) ;
#22283=PLANE ( 'NONE',  #31428 ) ;
#22333=FILL_AREA_STYLE_COLOUR ( '', #32839 ) ;
#22341=CARTESIAN_POINT ( 'NONE',  ( 5.000000000000000000, 2.342598717236900718, -4.057500000000001883 ) ) ;
#22347=VERTEX_POINT ( 'NONE', #8567 ) ;
#22361=FACE_OUTER_BOUND ( 'NONE', #22608, .T. ) ;
#22362=CYLINDRICAL_SURFACE ( 'NONE', #1839, 8.000000000000000000 ) ;
#22429=LINE ( 'NONE', #16814, #11795 ) ;
#22483=PRODUCT ( 'socket head cap screw_iso_ISO 4762 M10 x 90 - 32N', 'socket head cap screw_iso_ISO 4762 M10 x 90 - 32N', '', ( #25568 ) ) ;
#22485=CARTESIAN_POINT ( 'NONE',  ( 99.99999999999998579, 0.000000000000000000, 0.000000000000000000 ) ) ;
#22513=EDGE_CURVE ( 'NONE', #26329, #14311, #4459, .T. ) ;
#22553=CARTESIAN_POINT ( 'NONE',  ( 5.000000000000000000, 4.685197434473814759, -5.637851296924623057E-15 ) ) ;
#22562=VERTEX_POINT ( 'NONE', #27130 ) ;
#22608=EDGE_LOOP ( 'NONE', ( #9717, #14140, #29032, #1994 ) ) ;
#22646=ORIENTED_EDGE ( 'NONE', *, *, #15535, .F. ) ;
#22700=ADVANCED_FACE ( 'NONE', ( #23375 ), #1438, .F. ) ;
#22706=ORIENTED_EDGE ( 'NONE', *, *, #21622, .F. ) ;
#22756=DIRECTION ( 'NONE',  ( -0.7071067811865331398, 0.000000000000000000, 0.7071067811865620056 ) ) ;
#22871=EDGE_CURVE ( 'NONE', #29320, #26329, #5259, .T. ) ;
#22914=APPLICATION_CONTEXT ( 'automotive_design' ) ;
#22951=VERTEX_POINT ( 'NONE', #3243 ) ;
#22994=CARTESIAN_POINT ( 'NONE',  ( 0.000000000000000000, -2.342598717236903383, 4.057500000000001883 ) ) ;
#23019=VECTOR ( 'NONE', #12076, 1000.000000000000227 ) ;
#23094=( NAMED_UNIT ( * ) PLANE_ANGLE_UNIT ( ) SI_UNIT ( $, .RADIAN. ) );
#23102=DIRECTION ( 'NONE',  ( -1.000000000000000000, -0.000000000000000000, -0.000000000000000000 ) ) ;
#23226=CARTESIAN_POINT ( 'NONE',  ( 99.99999999999998579, 0.000000000000000000, 4.171999999999999709 ) ) ;
#23313=CARTESIAN_POINT ( 'NONE',  ( -31.74999999999995737, 0.000000000000000000, 5.000000000000001776 ) ) ;
#23375=FACE_OUTER_BOUND ( 'NONE', #7624, .T. ) ;
#23376=EDGE_LOOP ( 'NONE', ( #1542, #18719, #25332, #5353 ) ) ;
#23535=DIRECTION ( 'NONE',  ( -1.000000000000000000, -0.000000000000000000, -0.000000000000000000 ) ) ;
#23592=CARTESIAN_POINT ( 'NONE',  ( 10.40000000000000036, 6.123233995736768255E-16, -5.000000000000001776 ) ) ;
#23699=EDGE_CURVE ( 'NONE', #21974, #32863, #17784, .T. ) ;
#23741=EDGE_CURVE ( 'NONE', #11308, #8952, #22429, .T. ) ;
#23746=EDGE_CURVE ( 'NONE', #8952, #739, #29767, .T. ) ;
#23827=AXIS2_PLACEMENT_3D ( 'NONE', #25298, #25973, #14906 ) ;
#23851=CARTESIAN_POINT ( 'NONE',  ( 5.000000000000000000, -5.258101095580058680E-15, -4.057500000000000107 ) ) ;
#23861=ORIENTED_EDGE ( 'NONE', *, *, #15348, .T. ) ;
#23884=VECTOR ( 'NONE', #3051, 1000.000000000000000 ) ;
#23970=CARTESIAN_POINT ( 'NONE',  ( 10.00000000000000178, 0.000000000000000000, 8.000000000000000000 ) ) ;
#24090=VECTOR ( 'NONE', #9281, 999.9999999999998863 ) ;
#24128=( GEOMETRIC_REPRESENTATION_CONTEXT ( 3 ) GLOBAL_UNCERTAINTY_ASSIGNED_CONTEXT ( ( #32575 ) ) GLOBAL_UNIT_ASSIGNED_CONTEXT ( ( #1970, #25476, #33314 ) ) REPRESENTATION_CONTEXT ( 'NONE', 'WORKASPACE' ) );
#24164=EDGE_CURVE ( 'NONE', #8613, #20097, #7485, .T. ) ;
#24194=LINE ( 'NONE', #31534, #20337 ) ;
#24203=ORIENTED_EDGE ( 'NONE', *, *, #23699, .T. ) ;
#24270=CARTESIAN_POINT ( 'NONE',  ( 5.000000000000000000, 4.969004387540385421E-16, -4.057500000000000107 ) ) ;
#24272=DIRECTION ( 'NONE',  ( 0.000000000000000000, 0.000000000000000000, 1.000000000000000000 ) ) ;
#24314=ORIENTED_EDGE ( 'NONE', *, *, #30216, .F. ) ;
#24461=CIRCLE ( 'NONE', #33177, 0.4000000000000001887 ) ;
#24522=LINE ( 'NONE', #25189, #23019 ) ;
#24582=CIRCLE ( 'NONE', #9902, 6.500000000000000888 ) ;
#24596=ADVANCED_FACE ( 'NONE', ( #30241 ), #6899, .F. ) ;
#24662=ORIENTED_EDGE ( 'NONE', *, *, #24164, .T. ) ;
#24730=VECTOR ( 'NONE', #18368, 1000.000000000000000 ) ;
#24828=EDGE_LOOP ( 'NONE', ( #5263, #28700 ) ) ;
#24837=CIRCLE ( 'NONE', #28667, 5.400000000000002132 ) ;
#24893=( NAMED_UNIT ( * ) PLANE_ANGLE_UNIT ( ) SI_UNIT ( $, .RADIAN. ) );
#24954=DIRECTION ( 'NONE',  ( 0.000000000000000000, 0.4999999999999993339, -0.8660254037844389297 ) ) ;
#25014=DIRECTION ( 'NONE',  ( -0.000000000000000000, 0.8660254037844390407, 0.4999999999999993894 ) ) ;
#25046=FACE_OUTER_BOUND ( 'NONE', #7464, .T. ) ;
#25130=( NAMED_UNIT ( * ) SI_UNIT ( $, .STERADIAN. ) SOLID_ANGLE_UNIT ( ) );
#25153=EDGE_LOOP ( 'NONE', ( #10066, #14464, #17537 ) ) ;
#25169=VERTEX_POINT ( 'NONE', #15496 ) ;
#25172=FACE_OUTER_BOUND ( 'NONE', #25153, .T. ) ;
#25189=CARTESIAN_POINT ( 'NONE',  ( 5.000000000000000000, 4.685197434473814759, -5.637851296924623057E-15 ) ) ;
#25265=DIRECTION ( 'NONE',  ( 1.000000000000000000, 0.000000000000000000, 0.000000000000000000 ) ) ;
#25279=LINE ( 'NONE', #6546, #27141 ) ;
#25298=CARTESIAN_POINT ( 'NONE',  ( 10.40000000000000036, 0.000000000000000000, 0.000000000000000000 ) ) ;
#25306=SURFACE_STYLE_FILL_AREA ( #17642 ) ;
#25332=ORIENTED_EDGE ( 'NONE', *, *, #1661, .T. ) ;
#25476=( NAMED_UNIT ( * ) PLANE_ANGLE_UNIT ( ) SI_UNIT ( $, .RADIAN. ) );
#25507=CARTESIAN_POINT ( 'NONE',  ( 1.500000000000001332, 0.000000000000000000, 8.000000000000000000 ) ) ;
#25513=EDGE_LOOP ( 'NONE', ( #14717, #13228, #17203, #21477 ) ) ;
#25523=AXIS2_PLACEMENT_3D ( 'NONE', #30213, #25265, #19479 ) ;
#25539=EDGE_CURVE ( 'NONE', #8613, #1044, #31503, .T. ) ;
#25559=DIRECTION ( 'NONE',  ( 0.000000000000000000, 0.000000000000000000, 1.000000000000000000 ) ) ;
#25568=PRODUCT_CONTEXT ( 'NONE', #29421, 'mechanical' ) ;
#25629=EDGE_CURVE ( 'NONE', #13926, #26841, #11548, .T. ) ;
#25645=CARTESIAN_POINT ( 'NONE',  ( 99.99999999999998579, 0.000000000000000000, 4.171999999999999709 ) ) ;
#25724=CARTESIAN_POINT ( 'NONE',  ( 5.000000000000000000, 4.685197434473814759, -5.637851296924623057E-15 ) ) ;
#25772=( GEOMETRIC_REPRESENTATION_CONTEXT ( 3 ) GLOBAL_UNCERTAINTY_ASSIGNED_CONTEXT ( ( #3622 ) ) GLOBAL_UNIT_ASSIGNED_CONTEXT ( ( #9632, #23094, #25130 ) ) REPRESENTATION_CONTEXT ( 'NONE', 'WORKASPACE' ) );
#25778=CARTESIAN_POINT ( 'NONE',  ( 5.000000000000000000, 4.685197434473814759, -5.637851296924623057E-15 ) ) ;
#25905=CARTESIAN_POINT ( 'NONE',  ( 5.000000000000000000, 2.342598717236900718, -4.057500000000001883 ) ) ;
#25910=CIRCLE ( 'NONE', #30333, 4.057500000000000107 ) ;
#25971=VERTEX_POINT ( 'NONE', #25507 ) ;
#25973=DIRECTION ( 'NONE',  ( 1.000000000000000000, 0.000000000000000000, 0.000000000000000000 ) ) ;
#26222=PLANE ( 'NONE',  #7507 ) ;
#26302=MECHANICAL_DESIGN_GEOMETRIC_PRESENTATION_REPRESENTATION('',(#663),#24128);
#26329=VERTEX_POINT ( 'NONE', #16109 ) ;
#26349=UNCERTAINTY_MEASURE_WITH_UNIT (LENGTH_MEASURE( 1.000000000000000082E-05 ), #32551, 'distance_accuracy_value', 'NONE');
#26468=EDGE_LOOP ( 'NONE', ( #16555, #1536, #6768, #16817, #21760 ) ) ;
#26565=CARTESIAN_POINT ( 'NONE',  ( 5.000000000000000000, -2.342598717236912265, -4.057499999999995666 ) ) ;
#26572=CONICAL_SURFACE ( 'NONE', #20038, 4.171999999999999709, 0.7853981633974687071 ) ;
#26745=ORIENTED_EDGE ( 'NONE', *, *, #22871, .T. ) ;
#26810=CIRCLE ( 'NONE', #31706, 0.4000000000000001887 ) ;
#26841=VERTEX_POINT ( 'NONE', #23592 ) ;
#26882=DIRECTION ( 'NONE',  ( 1.000000000000000000, 0.000000000000000000, 0.000000000000000000 ) ) ;
#26910=LINE ( 'NONE', #26565, #7780 ) ;
#26966=DIRECTION ( 'NONE',  ( -1.000000000000000000, -0.000000000000000000, -0.000000000000000000 ) ) ;
#26980=VERTEX_POINT ( 'NONE', #10154 ) ;
#27120=DIRECTION ( 'NONE',  ( -1.000000000000000000, -0.000000000000000000, -0.000000000000000000 ) ) ;
#27130=CARTESIAN_POINT ( 'NONE',  ( 0.000000000000000000, 2.342598717236900718, -4.057500000000001883 ) ) ;
#27141=VECTOR ( 'NONE', #19831, 1000.000000000000000 ) ;
#27147=VECTOR ( 'NONE', #22756, 1000.000000000000000 ) ;
#27282=CARTESIAN_POINT ( 'NONE',  ( 0.000000000000000000, 0.000000000000000000, 0.000000000000000000 ) ) ;
#27307=ORIENTED_EDGE ( 'NONE', *, *, #2478, .T. ) ;
#27312=DIRECTION ( 'NONE',  ( -1.000000000000000000, -0.000000000000000000, -0.000000000000000000 ) ) ;
#27334=LINE ( 'NONE', #32613, #27881 ) ;
#27376=EDGE_LOOP ( 'NONE', ( #16528, #14946 ) ) ;
#27389=DIRECTION ( 'NONE',  ( 0.000000000000000000, 0.000000000000000000, -1.000000000000000000 ) ) ;
#27455=DIRECTION ( 'NONE',  ( 0.000000000000000000, 0.000000000000000000, -1.000000000000000000 ) ) ;
#27458=EDGE_LOOP ( 'NONE', ( #1439, #17937, #13067, #31865 ) ) ;
#27478=FACE_OUTER_BOUND ( 'NONE', #27965, .T. ) ;
#27497=CARTESIAN_POINT ( 'NONE',  ( 5.000000000000000000, -2.342598717236903383, 4.057500000000001883 ) ) ;
#27508=ORIENTED_EDGE ( 'NONE', *, *, #25629, .F. ) ;
#27713=CARTESIAN_POINT ( 'NONE',  ( 5.000000000000000000, 4.685197434473814759, -5.637851296924623057E-15 ) ) ;
#27724=ORIENTED_EDGE ( 'NONE', *, *, #1661, .F. ) ;
#27776=VECTOR ( 'NONE', #6280, 1000.000000000000000 ) ;
#27812=LINE ( 'NONE', #12149, #17928 ) ;
#27825=AXIS2_PLACEMENT_3D ( 'NONE', #19654, #32759, #30044 ) ;
#27881=VECTOR ( 'NONE', #24954, 1000.000000000000114 ) ;
#27965=EDGE_LOOP ( 'NONE', ( #3961, #18770, #10817, #10606 ) ) ;
#27989=DIRECTION ( 'NONE',  ( 0.000000000000000000, 0.000000000000000000, -1.000000000000000000 ) ) ;
#28055=ORIENTED_EDGE ( 'NONE', *, *, #8485, .F. ) ;
#28103=CARTESIAN_POINT ( 'NONE',  ( 5.000000000000000000, -3.513898075855363512, -2.028749999999998277 ) ) ;
#28137=EDGE_CURVE ( 'NONE', #22347, #2881, #3703, .T. ) ;
#28151=DIRECTION ( 'NONE',  ( 0.000000000000000000, 0.000000000000000000, 1.000000000000000000 ) ) ;
#28159=CARTESIAN_POINT ( 'NONE',  ( 5.000000000000000000, 2.342598717236910488, 4.057499999999995666 ) ) ;
#28207=SURFACE_SIDE_STYLE ('',( #25306 ) ) ;
#28360=LINE ( 'NONE', #15404, #16984 ) ;
#28367=VERTEX_POINT ( 'NONE', #14671 ) ;
#28457=CARTESIAN_POINT ( 'NONE',  ( 5.000000000000000000, -2.342598717236903383, 4.057500000000001883 ) ) ;
#28485=CARTESIAN_POINT ( 'NONE',  ( 5.000000000000000000, 0.000000000000000000, 0.000000000000000000 ) ) ;
#28533=ORIENTED_EDGE ( 'NONE', *, *, #17444, .F. ) ;
#28542=ORIENTED_EDGE ( 'NONE', *, *, #17467, .T. ) ;
#28557=CARTESIAN_POINT ( 'NONE',  ( 10.00000000000000178, 0.000000000000000000, 0.000000000000000000 ) ) ;
#28601=CARTESIAN_POINT ( 'NONE',  ( 99.99999999999998579, 5.616230220889761452E-16, -4.171999999999999709 ) ) ;
#28616=ORIENTED_EDGE ( 'NONE', *, *, #21858, .F. ) ;
#28667=AXIS2_PLACEMENT_3D ( 'NONE', #30549, #7211, #27989 ) ;
#28700=ORIENTED_EDGE ( 'NONE', *, *, #31044, .T. ) ;
#28790=EDGE_LOOP ( 'NONE', ( #15110, #13976, #30579, #31204, #31259 ) ) ;
#28802=DIRECTION ( 'NONE',  ( 0.000000000000000000, 1.000000000000000000, -1.295896757998781966E-15 ) ) ;
#28804=AXIS2_PLACEMENT_3D ( 'NONE', #9057, #9561, #27455 ) ;
#28885=EDGE_CURVE ( 'NONE', #13926, #31163, #10774, .T. ) ;
#28929=EDGE_CURVE ( 'NONE', #22951, #14728, #9345, .T. ) ;
#28944=ADVANCED_FACE ( 'NONE', ( #12413 ), #17358, .T. ) ;
#28999=VECTOR ( 'NONE', #17017, 1000.000000000000000 ) ;
#29032=ORIENTED_EDGE ( 'NONE', *, *, #30605, .F. ) ;
#29087=DIRECTION ( 'NONE',  ( -0.5000000000000034417, 0.000000000000000000, 0.8660254037844367092 ) ) ;
#29320=VERTEX_POINT ( 'NONE', #17865 ) ;
#29421=APPLICATION_CONTEXT ( 'automotive_design' ) ;
#29529=DIRECTION ( 'NONE',  ( 0.000000000000000000, 0.000000000000000000, -1.000000000000000000 ) ) ;
#29570=ORIENTED_EDGE ( 'NONE', *, *, #23741, .F. ) ;
#29633=LINE ( 'NONE', #16011, #27776 ) ;
#29686=DIRECTION ( 'NONE',  ( 0.000000000000000000, 0.000000000000000000, -1.000000000000000000 ) ) ;
#29752=DIRECTION ( 'NONE',  ( 0.000000000000000000, 0.000000000000000000, -1.000000000000000000 ) ) ;
#29767=LINE ( 'NONE', #8984, #16164 ) ;
#29782=DIRECTION ( 'NONE',  ( 0.000000000000000000, 0.000000000000000000, 1.000000000000000000 ) ) ;
#29797=AXIS2_PLACEMENT_3D ( 'NONE', #32966, #6744, #17468 ) ;
#29809=DIRECTION ( 'NONE',  ( 0.000000000000000000, 1.224646799147353207E-16, 1.000000000000000000 ) ) ;
#29821=EDGE_LOOP ( 'NONE', ( #29954, #15190, #4847, #12384, #18593 ) ) ;
#29858=DIRECTION ( 'NONE',  ( -1.000000000000000000, -0.000000000000000000, -0.000000000000000000 ) ) ;
#29906=LINE ( 'NONE', #24270, #24090 ) ;
#29954=ORIENTED_EDGE ( 'NONE', *, *, #20985, .T. ) ;
#29987=EDGE_CURVE ( 'NONE', #20097, #29320, #16253, .T. ) ;
#30015=DIRECTION ( 'NONE',  ( 0.000000000000000000, -0.5000000000000008882, -0.8660254037844381525 ) ) ;
#30028=CARTESIAN_POINT ( 'NONE',  ( 1.500000000000001332, 0.000000000000000000, 0.000000000000000000 ) ) ;
#30044=DIRECTION ( 'NONE',  ( 0.000000000000000000, 0.000000000000000000, 1.000000000000000000 ) ) ;
#30104=DIRECTION ( 'NONE',  ( 0.000000000000000000, -0.5000000000000014433, -0.8660254037844379305 ) ) ;
#30138=EDGE_CURVE ( 'NONE', #29320, #15495, #1226, .T. ) ;
#30189=ORIENTED_EDGE ( 'NONE', *, *, #6828, .T. ) ;
#30213=CARTESIAN_POINT ( 'NONE',  ( 5.000000000000000000, 4.685197434473814759, -5.637851296924623057E-15 ) ) ;
#30216=EDGE_CURVE ( 'NONE', #739, #22562, #6843, .T. ) ;
#30241=FACE_OUTER_BOUND ( 'NONE', #11512, .T. ) ;
#30333=AXIS2_PLACEMENT_3D ( 'NONE', #20504, #31241, #12835 ) ;
#30397=ORIENTED_EDGE ( 'NONE', *, *, #25539, .T. ) ;
#30409=AXIS2_PLACEMENT_3D ( 'NONE', #14193, #26966, #21692 ) ;
#30432=DIRECTION ( 'NONE',  ( 0.000000000000000000, 0.000000000000000000, 1.000000000000000000 ) ) ;
#30466=FACE_OUTER_BOUND ( 'NONE', #28790, .T. ) ;
#30549=CARTESIAN_POINT ( 'NONE',  ( 10.00000000000000178, 0.000000000000000000, 0.000000000000000000 ) ) ;
#30579=ORIENTED_EDGE ( 'NONE', *, *, #16616, .T. ) ;
#30605=EDGE_CURVE ( 'NONE', #5147, #25169, #14084, .T. ) ;
#30613=FACE_OUTER_BOUND ( 'NONE', #19422, .T. ) ;
#30655=CARTESIAN_POINT ( 'NONE',  ( 5.000000000000000000, 3.513898075855356851, -2.028750000000006271 ) ) ;
#30743=PLANE ( 'NONE',  #8833 ) ;
#30829=EDGE_CURVE ( 'NONE', #11134, #15698, #27812, .T. ) ;
#30856=DIRECTION ( 'NONE',  ( 0.000000000000000000, 0.000000000000000000, -1.000000000000000000 ) ) ;
#30875=CARTESIAN_POINT ( 'NONE',  ( 7.342598717236928252, 0.000000000000000000, 0.000000000000000000 ) ) ;
#30929=ADVANCED_FACE ( 'NONE', ( #9425 ), #19819, .F. ) ;
#30932=ORIENTED_EDGE ( 'NONE', *, *, #23699, .F. ) ;
#30944=DIRECTION ( 'NONE',  ( 0.000000000000000000, 0.000000000000000000, 1.000000000000000000 ) ) ;
#31044=EDGE_CURVE ( 'NONE', #25169, #5147, #24837, .T. ) ;
#31143=PRODUCT_DEFINITION_FORMATION_WITH_SPECIFIED_SOURCE ( 'ANY', '', #22483, .NOT_KNOWN. ) ;
#31160=VECTOR ( 'NONE', #4159, 1000.000000000000000 ) ;
#31163=VERTEX_POINT ( 'NONE', #1002 ) ;
#31204=ORIENTED_EDGE ( 'NONE', *, *, #13973, .T. ) ;
#31241=DIRECTION ( 'NONE',  ( -1.000000000000000000, -0.000000000000000000, -0.000000000000000000 ) ) ;
#31259=ORIENTED_EDGE ( 'NONE', *, *, #32404, .T. ) ;
#31266=ORIENTED_EDGE ( 'NONE', *, *, #32471, .T. ) ;
#31386=LINE ( 'NONE', #33609, #12616 ) ;
#31395=ADVANCED_FACE ( 'NONE', ( #25172 ), #17345, .F. ) ;
#31428=AXIS2_PLACEMENT_3D ( 'NONE', #6611, #19723, #27389 ) ;
#31503=LINE ( 'NONE', #8330, #6988 ) ;
#31534=CARTESIAN_POINT ( 'NONE',  ( 5.000000000000000000, -4.685197434473814759, 3.903127820947815962E-15 ) ) ;
#31566=FACE_OUTER_BOUND ( 'NONE', #25513, .T. ) ;
#31706=AXIS2_PLACEMENT_3D ( 'NONE', #11297, #19294, #29686 ) ;
#31731=CIRCLE ( 'NONE', #11068, 8.000000000000000000 ) ;
#31865=ORIENTED_EDGE ( 'NONE', *, *, #31044, .F. ) ;
#31921=AXIS2_PLACEMENT_3D ( 'NONE', #21428, #8479, #16311 ) ;
#31982=AXIS2_PLACEMENT_3D ( 'NONE', #1014, #32178, #8838 ) ;
#32085=ORIENTED_EDGE ( 'NONE', *, *, #32471, .F. ) ;
#32149=AXIS2_PLACEMENT_3D ( 'NONE', #17683, #25014, #9674 ) ;
#32178=DIRECTION ( 'NONE',  ( -1.000000000000000000, -0.000000000000000000, -0.000000000000000000 ) ) ;
#32235=ORIENTED_EDGE ( 'NONE', *, *, #23741, .T. ) ;
#32245=DIRECTION ( 'NONE',  ( 1.000000000000000000, 0.000000000000000000, 0.000000000000000000 ) ) ;
#32288=CIRCLE ( 'NONE', #32818, 4.057500000000000107 ) ;
#32304=CARTESIAN_POINT ( 'NONE',  ( 5.000000000000000000, 0.000000000000000000, 4.057500000000000107 ) ) ;
#32393=FACE_OUTER_BOUND ( 'NONE', #1650, .T. ) ;
#32404=EDGE_CURVE ( 'NONE', #1044, #3872, #26910, .T. ) ;
#32424=DIRECTION ( 'NONE',  ( -1.000000000000000000, -0.000000000000000000, -0.000000000000000000 ) ) ;
#32433=DIRECTION ( 'NONE',  ( -1.000000000000000000, -0.000000000000000000, -0.000000000000000000 ) ) ;
#32471=EDGE_CURVE ( 'NONE', #11308, #26980, #24522, .T. ) ;
#32514=DIRECTION ( 'NONE',  ( 1.000000000000000000, 0.000000000000000000, 0.000000000000000000 ) ) ;
#32551=( LENGTH_UNIT ( ) NAMED_UNIT ( * ) SI_UNIT ( .MILLI., .METRE. ) );
#32575=UNCERTAINTY_MEASURE_WITH_UNIT (LENGTH_MEASURE( 1.000000000000000082E-05 ), #1970, 'distance_accuracy_value', 'NONE');
#32613=CARTESIAN_POINT ( 'NONE',  ( 0.000000000000000000, -4.685197434473814759, 3.903127820947815962E-15 ) ) ;
#32627=EDGE_CURVE ( 'NONE', #20140, #11974, #1856, .T. ) ;
#32663=CARTESIAN_POINT ( 'NONE',  ( 99.99999999999998579, 0.000000000000000000, 0.000000000000000000 ) ) ;
#32702=EDGE_LOOP ( 'NONE', ( #16691, #28533, #10887, #3765, #23861 ) ) ;
#32707=ORIENTED_EDGE ( 'NONE', *, *, #28929, .F. ) ;
#32720=SURFACE_STYLE_FILL_AREA ( #19783 ) ;
#32733=DIRECTION ( 'NONE',  ( 0.000000000000000000, 0.000000000000000000, 1.000000000000000000 ) ) ;
#32750=CARTESIAN_POINT ( 'NONE',  ( 5.000000000000000000, -2.342598717236903383, 4.057500000000001883 ) ) ;
#32751=CARTESIAN_POINT ( 'NONE',  ( -31.74999999999995737, 0.000000000000000000, 0.000000000000000000 ) ) ;
#32759=DIRECTION ( 'NONE',  ( -1.000000000000000000, -0.000000000000000000, -0.000000000000000000 ) ) ;
#32818=AXIS2_PLACEMENT_3D ( 'NONE', #8089, #18799, #408 ) ;
#32839=COLOUR_RGB ( '', 0.31764706, 0.68627451, 0.89019608) ;
#32863=VERTEX_POINT ( 'NONE', #28601 ) ;
#32925=DIRECTION ( 'NONE',  ( 0.000000000000000000, 0.5000000000000008882, 0.8660254037844381525 ) ) ;
#32947=ORIENTED_EDGE ( 'NONE', *, *, #21622, .T. ) ;
#32951=CARTESIAN_POINT ( 'NONE',  ( 5.000000000000000000, 2.342598717236910488, 4.057499999999995666 ) ) ;
#32957=DIRECTION ( 'NONE',  ( 0.000000000000000000, 0.5000000000000014433, 0.8660254037844379305 ) ) ;
#32966=CARTESIAN_POINT ( 'NONE',  ( 10.40000000000000036, 0.000000000000000000, 0.000000000000000000 ) ) ;
#33005=DIRECTION ( 'NONE',  ( 1.000000000000000000, 0.000000000000000000, 0.000000000000000000 ) ) ;
#33108=CARTESIAN_POINT ( 'NONE',  ( 0.000000000000000000, -2.342598717236912265, -4.057499999999995666 ) ) ;
#33177=AXIS2_PLACEMENT_3D ( 'NONE', #6286, #14635, #29809 ) ;
#33238=SURFACE_STYLE_USAGE ( .BOTH. , #17055 ) ;
#33314=( NAMED_UNIT ( * ) SI_UNIT ( $, .STERADIAN. ) SOLID_ANGLE_UNIT ( ) );
#33490=DIRECTION ( 'NONE',  ( 0.000000000000000000, 0.000000000000000000, 1.000000000000000000 ) ) ;
#33520=ORIENTED_EDGE ( 'NONE', *, *, #17444, .T. ) ;
#33565=DIRECTION ( 'NONE',  ( 0.000000000000000000, 0.4999999999999994449, -0.8660254037844389297 ) ) ;
#33573=SHAPE_DEFINITION_REPRESENTATION ( #12151, #1289 ) ;
#33601=VECTOR ( 'NONE', #32424, 1000.000000000000000 ) ;
#33609=CARTESIAN_POINT ( 'NONE',  ( 0.000000000000000000, 4.685197434473814759, -5.637851296924623057E-15 ) ) ;
#33642=CIRCLE ( 'NONE', #22198, 1.499999999999999556 ) ;
#33651=LINE ( 'NONE', #25645, #27147 ) ;
ENDSEC;
END-ISO-10303-21;
